ISO-10303-21;
HEADER;
/* Generated by software containing ST-Developer
 * from STEP Tools, Inc. (www.steptools.com) 
 */

FILE_DESCRIPTION(
/* description */ ('STEP AP214'),
/* implementation_level */ '2;1');

FILE_NAME(
/* name */ 'BO21-001_Ball_D3.5 Steel Ball.step',
/* time_stamp */ '2026-10-07T12:49:37-07:00',
/* author */ (''),
/* organization */ (''),
/* preprocessor_version */ 'ST-DEVELOPER v20.2',
/* originating_system */ 'Autodesk Translation Framework v15.15.0.0',
/* authorisation */ '');

FILE_SCHEMA (('AUTOMOTIVE_DESIGN { 1 0 10303 214 3 1 1 }'));
ENDSEC;

DATA;
#10=MECHANICAL_DESIGN_GEOMETRIC_PRESENTATION_REPRESENTATION('',(#314),#33016);
#180=SPHERICAL_SURFACE('',#11148,1.75);
#256=SHAPE_REPRESENTATION_RELATIONSHIP('SRR','None',#33151,#283);
#283=ADVANCED_BREP_SHAPE_REPRESENTATION('',(#341),#33012);
#314=STYLED_ITEM('',(#33286),#341);
#341=MANIFOLD_SOLID_BREP('Body1',#9965);
#1542=FACE_OUTER_BOUND('',#2174,.T.);
#2174=EDGE_LOOP('',(#9064,#9065));
#2571=CIRCLE('',#11149,1.75);
#4972=VERTEX_POINT('',#32718);
#4973=VERTEX_POINT('',#32719);
#6345=EDGE_CURVE('',#4972,#4973,#2571,.T.);
#9064=ORIENTED_EDGE('',*,*,#6345,.T.);
#9065=ORIENTED_EDGE('',*,*,#6345,.F.);
#9908=ADVANCED_FACE('',(#1542),#180,.T.);
#9965=CLOSED_SHELL('',(#9908));
#11147=AXIS2_PLACEMENT_3D('',#32716,#13717,#13718);
#11148=AXIS2_PLACEMENT_3D('',#32717,#13719,#13720);
#11149=AXIS2_PLACEMENT_3D('',#32720,#13721,#13722);
#13717=DIRECTION('axis',(0.,0.,1.));
#13718=DIRECTION('refdir',(1.,0.,0.));
#13719=DIRECTION('center_axis',(-1.,1.11022302462515E-16,6.12323399573677E-17));
#13720=DIRECTION('ref_axis',(0.,0.,1.));
#13721=DIRECTION('center_axis',(-1.11022302462515E-16,-1.,1.22464679914735E-16));
#13722=DIRECTION('ref_axis',(-1.35963107344689E-32,-1.22464679914735E-16,
-1.));
#32716=CARTESIAN_POINT('',(0.,0.,0.));
#32717=CARTESIAN_POINT('Origin',(0.,0.,0.));
#32718=CARTESIAN_POINT('',(-1.75,1.94289029309402E-16,-1.07156594925393E-16));
#32719=CARTESIAN_POINT('',(1.75,-1.94289029309402E-16,-1.07156594925393E-16));
#32720=CARTESIAN_POINT('Origin',(0.,0.,0.));
#32980=UNCERTAINTY_MEASURE_WITH_UNIT(LENGTH_MEASURE(0.01),#33017,
'DISTANCE_ACCURACY_VALUE',
'Maximum model space distance between geometric entities at asserted c
onnectivities');
#32984=UNCERTAINTY_MEASURE_WITH_UNIT(LENGTH_MEASURE(0.01),#33017,
'DISTANCE_ACCURACY_VALUE',
'Maximum model space distance between geometric entities at asserted c
onnectivities');
#33012=(
GEOMETRIC_REPRESENTATION_CONTEXT(3)
GLOBAL_UNCERTAINTY_ASSIGNED_CONTEXT((#32980))
GLOBAL_UNIT_ASSIGNED_CONTEXT((#33017,#33019,#33020))
REPRESENTATION_CONTEXT('','3D')
);
#33016=(
GEOMETRIC_REPRESENTATION_CONTEXT(3)
GLOBAL_UNCERTAINTY_ASSIGNED_CONTEXT((#32984))
GLOBAL_UNIT_ASSIGNED_CONTEXT((#33017,#33019,#33020))
REPRESENTATION_CONTEXT('','3D')
);
#33017=(
LENGTH_UNIT()
NAMED_UNIT(*)
SI_UNIT(.MILLI.,.METRE.)
);
#33019=(
NAMED_UNIT(*)
PLANE_ANGLE_UNIT()
SI_UNIT($,.RADIAN.)
);
#33020=(
NAMED_UNIT(*)
SI_UNIT($,.STERADIAN.)
SOLID_ANGLE_UNIT()
);
#33048=SHAPE_DEFINITION_REPRESENTATION(#33101,#33151);
#33101=PRODUCT_DEFINITION_SHAPE('',$,#33183);
#33151=SHAPE_REPRESENTATION('',(#11147),#33012);
#33155=PRODUCT_DEFINITION_CONTEXT('part definition',#33250,'design');
#33183=PRODUCT_DEFINITION('BO21-001_Ball_D3.5 Steel Ball',
'BO21-001_Ball_D3.5 Steel Ball',#33214,#33155);
#33214=PRODUCT_DEFINITION_FORMATION('',$,#33279);
#33250=APPLICATION_CONTEXT(
'Core Data for Automotive Mechanical Design Process');
#33251=PRODUCT_CONTEXT('part definition',#33250,'mechanical');
#33279=PRODUCT('BO21-001_Ball_D3.5 Steel Ball',
'BO21-001_Ball_D3.5 Steel Ball',$,(#33251));
#33286=PRESENTATION_STYLE_ASSIGNMENT((#33293));
#33293=SURFACE_STYLE_USAGE(.BOTH.,#33300);
#33300=SURFACE_SIDE_STYLE('',(#33307));
#33307=SURFACE_STYLE_FILL_AREA(#33314);
#33314=FILL_AREA_STYLE('Opaque(178,178,178)',(#33321));
#33321=FILL_AREA_STYLE_COLOUR('Opaque(178,178,178)',#33328);
#33328=COLOUR_RGB('Opaque(178,178,178)', 0.66274510, 0.83137255, 0.94901961);
ENDSEC;
END-ISO-10303-21;
